ISO-10303-21;
HEADER;
FILE_DESCRIPTION (('STEP AP214'),
    '1' );
FILE_NAME ('Rubber Head.step',
    '2026-10-06T08:09:25',
    ( '' ),
    ( '' ),
    'SwSTEP 2.0',
    'SolidWorks 2021',
    '' );
FILE_SCHEMA (( 'AUTOMOTIVE_DESIGN' ));
ENDSEC;

DATA;
#100=CARTESIAN_POINT ( 'NONE',  ( -6.938893903907228378E-15, -22.91099746826335348, -1.387778780781445676E-14 ) ) ;
#162=DIRECTION ( 'NONE',  ( 2.172745813409349776E-17, -1.000000000000000000, 1.309377075419428048E-16 ) ) ;
#202=ADVANCED_BREP_SHAPE_REPRESENTATION ( '', ( #21257, #21014, #22115 ), #20270 ) ;
#212=DIRECTION ( 'NONE',  ( -2.172745813409349776E-17, 1.000000000000000000, -1.309377075419428048E-16 ) ) ;
#267=STYLED_ITEM ( 'NONE', ( #8597 ), #21014 ) ;
#401=AXIS2_PLACEMENT_3D ( 'NONE', #4614, #22620, #18981 ) ;
#437=LINE ( 'NONE', #1953, #9814 ) ;
#480=CONICAL_SURFACE ( 'NONE', #22650, 4.750000000000013323, 0.6593100683328582123 ) ;
#530=ADVANCED_FACE ( 'NONE', ( #14233 ), #19524, .T. ) ;
#628=ORIENTED_EDGE ( 'NONE', *, *, #21380, .F. ) ;
#648=FACE_OUTER_BOUND ( 'NONE', #10629, .T. ) ;
#714=EDGE_LOOP ( 'NONE', ( #13357, #3608, #9239, #4112 ) ) ;
#743=ORIENTED_EDGE ( 'NONE', *, *, #17717, .F. ) ;
#860=ORIENTED_EDGE ( 'NONE', *, *, #3116, .T. ) ;
#907=DIRECTION ( 'NONE',  ( 9.470910429910634558E-17, 0.000000000000000000, -1.000000000000000000 ) ) ;
#963=CARTESIAN_POINT ( 'NONE',  ( 0.000000000000000000, 0.000000000000000000, 0.000000000000000000 ) ) ;
#1095=DIRECTION ( 'NONE',  ( -2.775557561562883647E-17, 3.406761633869147840E-16, -1.000000000000000000 ) ) ;
#1397=CARTESIAN_POINT ( 'NONE',  ( 0.000000000000000000, -14.99999999999997513, -1.387778780781445676E-14 ) ) ;
#1502=DIRECTION ( 'NONE',  ( 1.091943820671237506E-16, -0.7904150521752423275, 0.6125716654358156488 ) ) ;
#1583=CIRCLE ( 'NONE', #2335, 12.14055452724117856 ) ;
#1607=ORIENTED_EDGE ( 'NONE', *, *, #14971, .F. ) ;
#1626=PLANE ( 'NONE',  #11219 ) ;
#1627=( LENGTH_UNIT ( ) NAMED_UNIT ( * ) SI_UNIT ( .MILLI., .METRE. ) );
#1673=AXIS2_PLACEMENT_3D ( 'NONE', #18535, #5961, #3950 ) ;
#1772=( GEOMETRIC_REPRESENTATION_CONTEXT ( 3 ) GLOBAL_UNCERTAINTY_ASSIGNED_CONTEXT ( ( #4602 ) ) GLOBAL_UNIT_ASSIGNED_CONTEXT ( ( #19888, #7082, #5068 ) ) REPRESENTATION_CONTEXT ( 'NONE', 'WORKASPACE' ) );
#1791=DIRECTION ( 'NONE',  ( 2.172745813409349776E-17, -1.000000000000000000, 1.309377075419428048E-16 ) ) ;
#1804=AXIS2_PLACEMENT_3D ( 'NONE', #15904, #4974, #22755 ) ;
#1815=VECTOR ( 'NONE', #2710, 1000.000000000000227 ) ;
#1924=DIRECTION ( 'NONE',  ( -1.000000000000000000, -2.172745813409349776E-17, 2.775557561562883647E-17 ) ) ;
#1953=CARTESIAN_POINT ( 'NONE',  ( -1.316424159404522588E-14, -24.99999999999998224, 4.750000000000013323 ) ) ;
#2002=ORIENTED_EDGE ( 'NONE', *, *, #11745, .T. ) ;
#2073=DIRECTION ( 'NONE',  ( -2.775557561562824791E-17, 0.000000000000000000, -1.000000000000000000 ) ) ;
#2095=DIRECTION ( 'NONE',  ( 2.775557561562883647E-17, -3.652049423109057473E-16, 1.000000000000000000 ) ) ;
#2134=MECHANICAL_DESIGN_GEOMETRIC_PRESENTATION_REPRESENTATION('',(#267),#1772);
#2169=CIRCLE ( 'NONE', #13446, 2.500000000000006661 ) ;
#2283=FACE_OUTER_BOUND ( 'NONE', #10429, .T. ) ;
#2293=VERTEX_POINT ( 'NONE', #3164 ) ;
#2303=CYLINDRICAL_SURFACE ( 'NONE', #18883, 2.500000000000006661 ) ;
#2317=AXIS2_PLACEMENT_3D ( 'NONE', #19356, #17586, #13603 ) ;
#2335=AXIS2_PLACEMENT_3D ( 'NONE', #17855, #17973, #21402 ) ;
#2501=DIRECTION ( 'NONE',  ( -2.775557561562883647E-17, 3.406761633869147840E-16, -1.000000000000000000 ) ) ;
#2526=VERTEX_POINT ( 'NONE', #9485 ) ;
#2534=AXIS2_PLACEMENT_3D ( 'NONE', #13114, #9701, #5840 ) ;
#2539=CYLINDRICAL_SURFACE ( 'NONE', #15084, 4.750000000000013323 ) ;
#2609=MECHANICAL_DESIGN_GEOMETRIC_PRESENTATION_REPRESENTATION('',(#16115),#19899);
#2658=EDGE_CURVE ( 'NONE', #13530, #16493, #11950, .T. ) ;
#2710=DIRECTION ( 'NONE',  ( -5.861751848416504610E-18, 0.9863939238321435266, -0.1643989873053580686 ) ) ;
#2738=CIRCLE ( 'NONE', #15498, 2.500000000000000444 ) ;
#2880=VERTEX_POINT ( 'NONE', #12280 ) ;
#2905=ADVANCED_FACE ( 'NONE', ( #8648 ), #22118, .T. ) ;
#2963=DIRECTION ( 'NONE',  ( 0.000000000000000000, 0.000000000000000000, 1.000000000000000000 ) ) ;
#3030=ADVANCED_FACE ( 'NONE', ( #2283 ), #5219, .T. ) ;
#3038=ADVANCED_FACE ( 'NONE', ( #648 ), #21387, .T. ) ;
#3116=EDGE_CURVE ( 'NONE', #21123, #2526, #11919, .T. ) ;
#3164=CARTESIAN_POINT ( 'NONE',  ( 2.869123094150544522E-16, -14.99999999999997513, -4.750000000000013323 ) ) ;
#3233=EDGE_LOOP ( 'NONE', ( #16430, #6729, #15172, #743 ) ) ;
#3260=ORIENTED_EDGE ( 'NONE', *, *, #6238, .T. ) ;
#3268=ORIENTED_EDGE ( 'NONE', *, *, #21927, .T. ) ;
#3280=CIRCLE ( 'NONE', #5528, 2.500000000000000444 ) ;
#3295=EDGE_LOOP ( 'NONE', ( #11091, #15247, #11211, #13649 ) ) ;
#3297=CARTESIAN_POINT ( 'NONE',  ( 0.000000000000000000, -14.99999999999997513, -1.387778780781445676E-14 ) ) ;
#3381=DIRECTION ( 'NONE',  ( 2.775557561562883955E-17, -3.406761633869148333E-16, 1.000000000000000000 ) ) ;
#3424=DIRECTION ( 'NONE',  ( -2.775557561562883647E-17, 3.652049423109057473E-16, -1.000000000000000000 ) ) ;
#3432=ORIENTED_EDGE ( 'NONE', *, *, #18423, .T. ) ;
#3448=PRODUCT_DEFINITION ( 'UNKNOWN', '', #18771, #20179 ) ;
#3476=DIRECTION ( 'NONE',  ( -2.172745813409349776E-17, 1.000000000000000000, -1.309377075419428048E-16 ) ) ;
#3512=FACE_OUTER_BOUND ( 'NONE', #14015, .T. ) ;
#3515=ORIENTED_EDGE ( 'NONE', *, *, #2658, .F. ) ;
#3544=CONICAL_SURFACE ( 'NONE', #1673, 12.50000000000003375, 0.1651486774146268266 ) ;
#3566=CYLINDRICAL_SURFACE ( 'NONE', #7319, 4.750000000000013323 ) ;
#3567=CARTESIAN_POINT ( 'NONE',  ( 2.081668171172168513E-14, 10.00000000000000533, 0.000000000000000000 ) ) ;
#3608=ORIENTED_EDGE ( 'NONE', *, *, #5772, .T. ) ;
#3615=EDGE_CURVE ( 'NONE', #10242, #15995, #2169, .T. ) ;
#3697=CARTESIAN_POINT ( 'NONE',  ( 1.477270212546007475E-14, -24.99999999999998224, -7.882182279042408979 ) ) ;
#3792=AXIS2_PLACEMENT_3D ( 'NONE', #100, #212, #11012 ) ;
#3810=DIRECTION ( 'NONE',  ( 2.775557561562831570E-17, 0.000000000000000000, 1.000000000000000000 ) ) ;
#3813=LINE ( 'NONE', #12404, #12902 ) ;
#3822=ORIENTED_EDGE ( 'NONE', *, *, #13750, .F. ) ;
#3829=FACE_OUTER_BOUND ( 'NONE', #16269, .T. ) ;
#3832=CARTESIAN_POINT ( 'NONE',  ( 2.081668171172168513E-14, 10.00000000000000533, 0.000000000000000000 ) ) ;
#3871=CARTESIAN_POINT ( 'NONE',  ( -1.318389841742373392E-16, -14.99999999999997335, -4.750000000000026645 ) ) ;
#3918=DIRECTION ( 'NONE',  ( 2.172745813409349776E-17, -1.000000000000000000, 1.309377075419428048E-16 ) ) ;
#3919=EDGE_CURVE ( 'NONE', #19599, #16893, #18377, .T. ) ;
#3950=DIRECTION ( 'NONE',  ( 2.775557561562886113E-17, -2.775557561562883955E-16, 1.000000000000000000 ) ) ;
#4050=CIRCLE ( 'NONE', #1804, 4.999999999999999112 ) ;
#4112=ORIENTED_EDGE ( 'NONE', *, *, #21745, .F. ) ;
#4133=ADVANCED_FACE ( 'NONE', ( #7704 ), #22055, .F. ) ;
#4149=DIRECTION ( 'NONE',  ( 2.172745813409349776E-17, -1.000000000000000000, 1.309377075419428048E-16 ) ) ;
#4237=AXIS2_PLACEMENT_3D ( 'NONE', #3567, #12608, #11191 ) ;
#4386=AXIS2_PLACEMENT_3D ( 'NONE', #10331, #6585, #17030 ) ;
#4427=ORIENTED_EDGE ( 'NONE', *, *, #11745, .F. ) ;
#4464=DIRECTION ( 'NONE',  ( 2.775557561562885188E-17, 1.309377075419427801E-16, 1.000000000000000000 ) ) ;
#4534=DIRECTION ( 'NONE',  ( 1.000000000000000000, 2.172745813409351317E-17, 9.470910429910635790E-17 ) ) ;
#4574=DIRECTION ( 'NONE',  ( -2.172745813409349776E-17, 1.000000000000000000, -1.309377075419428048E-16 ) ) ;
#4589=LINE ( 'NONE', #6483, #1815 ) ;
#4602=UNCERTAINTY_MEASURE_WITH_UNIT (LENGTH_MEASURE( 1.000000000000000082E-05 ), #19888, 'distance_accuracy_value', 'NONE');
#4614=CARTESIAN_POINT ( 'NONE',  ( 0.000000000000000000, 0.000000000000000000, 0.000000000000000000 ) ) ;
#4638=CIRCLE ( 'NONE', #20436, 4.750000000000013323 ) ;
#4889=CARTESIAN_POINT ( 'NONE',  ( 2.869123094150540578E-16, -6.219541108242227082E-16, -4.750000000000000000 ) ) ;
#4943=CARTESIAN_POINT ( 'NONE',  ( 0.000000000000000000, 0.000000000000000000, 0.000000000000000000 ) ) ;
#4974=DIRECTION ( 'NONE',  ( -1.000000000000000000, -2.172745813409349776E-17, 2.775557561562883647E-17 ) ) ;
#4975=CARTESIAN_POINT ( 'NONE',  ( 1.462430223138485341E-14, -22.49999999999995381, -7.882182279042456940 ) ) ;
#4976=PRODUCT ( 'Rubber Head', 'Rubber Head', '', ( #10712 ) ) ;
#5042=VERTEX_POINT ( 'NONE', #21130 ) ;
#5068=( NAMED_UNIT ( * ) SI_UNIT ( $, .STERADIAN. ) SOLID_ANGLE_UNIT ( ) );
#5104=ORIENTED_EDGE ( 'NONE', *, *, #16137, .F. ) ;
#5117=MECHANICAL_DESIGN_GEOMETRIC_PRESENTATION_REPRESENTATION('',(#12233),#22025);
#5153=CARTESIAN_POINT ( 'NONE',  ( 0.000000000000000000, 0.000000000000000000, 0.000000000000000000 ) ) ;
#5219=TOROIDAL_SURFACE ( 'NONE', #8221, 7.208584908080424292, 5.000000000000000000 ) ;
#5288=EDGE_LOOP ( 'NONE', ( #5586, #8419, #16769, #18267 ) ) ;
#5306=DIRECTION ( 'NONE',  ( 1.000000000000000000, 0.000000000000000000, 0.000000000000000000 ) ) ;
#5428=AXIS2_PLACEMENT_3D ( 'NONE', #17670, #162, #12609 ) ;
#5450=CARTESIAN_POINT ( 'NONE',  ( 2.085593006335308133E-14, 10.00000000000000533, -2.500000000000000000 ) ) ;
#5473=DIRECTION ( 'NONE',  ( 2.775557561562886729E-17, -4.401632478328199173E-16, 1.000000000000000000 ) ) ;
#5494=ORIENTED_EDGE ( 'NONE', *, *, #9228, .T. ) ;
#5528=AXIS2_PLACEMENT_3D ( 'NONE', #4975, #15672, #6868 ) ;
#5537=CARTESIAN_POINT ( 'NONE',  ( 0.000000000000000000, -14.99999999999997513, -1.387778780781445676E-14 ) ) ;
#5562=FACE_OUTER_BOUND ( 'NONE', #3295, .T. ) ;
#5564=CYLINDRICAL_SURFACE ( 'NONE', #5428, 4.750000000000013323 ) ;
#5586=ORIENTED_EDGE ( 'NONE', *, *, #9228, .F. ) ;
#5608=AXIS2_PLACEMENT_3D ( 'NONE', #7360, #3476, #17836 ) ;
#5690=( NAMED_UNIT ( * ) SI_UNIT ( $, .STERADIAN. ) SOLID_ANGLE_UNIT ( ) );
#5692=CIRCLE ( 'NONE', #6812, 7.882182279042429407 ) ;
#5772=EDGE_CURVE ( 'NONE', #14225, #13530, #4589, .T. ) ;
#5775=CIRCLE ( 'NONE', #21564, 11.16066016895667268 ) ;
#5830=CARTESIAN_POINT ( 'NONE',  ( 2.085593006335303400E-14, -3.273442688548351087E-16, -2.500000000000000000 ) ) ;
#5840=DIRECTION ( 'NONE',  ( 2.775557561562883955E-17, -3.406761633869148826E-16, 1.000000000000000000 ) ) ;
#5961=DIRECTION ( 'NONE',  ( -2.172745813409349776E-17, 1.000000000000000000, -1.309377075419428048E-16 ) ) ;
#6033=( NAMED_UNIT ( * ) PLANE_ANGLE_UNIT ( ) SI_UNIT ( $, .RADIAN. ) );
#6102=CARTESIAN_POINT ( 'NONE',  ( -1.318389841742373392E-16, 1.618211776087849834E-15, -4.750000000000013323 ) ) ;
#6152=ORIENTED_EDGE ( 'NONE', *, *, #16137, .T. ) ;
#6172=EDGE_CURVE ( 'NONE', #5042, #16493, #16786, .T. ) ;
#6238=EDGE_CURVE ( 'NONE', #19599, #15995, #17622, .T. ) ;
#6271=ORIENTED_EDGE ( 'NONE', *, *, #22175, .F. ) ;
#6285=ADVANCED_FACE ( 'NONE', ( #3512 ), #1626, .F. ) ;
#6426=DIRECTION ( 'NONE',  ( -2.775557561562883955E-17, 3.406761633869148826E-16, -1.000000000000000000 ) ) ;
#6483=CARTESIAN_POINT ( 'NONE',  ( -5.755030100168395711E-15, -9.999999999999964473, -12.50000000000003375 ) ) ;
#6545=DIRECTION ( 'NONE',  ( 2.172745813409349776E-17, -1.000000000000000000, 1.309377075419428048E-16 ) ) ;
#6585=DIRECTION ( 'NONE',  ( -2.172745813409349776E-17, 1.000000000000000000, -1.309377075419428048E-16 ) ) ;
#6729=ORIENTED_EDGE ( 'NONE', *, *, #9603, .T. ) ;
#6744=COLOUR_RGB ( '', 0.08235294, 0.09019608, 0.10196078) ;
#6812=AXIS2_PLACEMENT_3D ( 'NONE', #8309, #16761, #20437 ) ;
#6868=DIRECTION ( 'NONE',  ( 9.470910429910671536E-17, 0.000000000000000000, -1.000000000000000000 ) ) ;
#7017=DIRECTION ( 'NONE',  ( -2.775557561562883647E-17, 3.406761633869147840E-16, -1.000000000000000000 ) ) ;
#7066=DIRECTION ( 'NONE',  ( -2.172745813409348851E-17, 1.000000000000000000, 3.406761633869148826E-16 ) ) ;
#7082=( NAMED_UNIT ( * ) PLANE_ANGLE_UNIT ( ) SI_UNIT ( $, .RADIAN. ) );
#7169=FILL_AREA_STYLE ('',( #17739 ) ) ;
#7186=DIRECTION ( 'NONE',  ( 2.775557561562891043E-17, -3.108639542312977099E-16, 1.000000000000000000 ) ) ;
#7319=AXIS2_PLACEMENT_3D ( 'NONE', #12728, #1791, #16128 ) ;
#7329=CARTESIAN_POINT ( 'NONE',  ( 2.130086964121806377E-14, 10.00000000000000533, 2.500000000000000000 ) ) ;
#7360=CARTESIAN_POINT ( 'NONE',  ( 2.081668171172168513E-14, 10.00000000000000533, 0.000000000000000000 ) ) ;
#7407=ORIENTED_EDGE ( 'NONE', *, *, #17149, .T. ) ;
#7452=( NAMED_UNIT ( * ) SI_UNIT ( $, .STERADIAN. ) SOLID_ANGLE_UNIT ( ) );
#7488=FACE_OUTER_BOUND ( 'NONE', #714, .T. ) ;
#7535=VECTOR ( 'NONE', #16356, 1000.000000000000000 ) ;
#7568=VERTEX_POINT ( 'NONE', #7619 ) ;
#7599=ORIENTED_EDGE ( 'NONE', *, *, #22939, .F. ) ;
#7619=CARTESIAN_POINT ( 'NONE',  ( -1.365901330155232488E-14, -24.99999999999998579, 7.882182279042429407 ) ) ;
#7698=CARTESIAN_POINT ( 'NONE',  ( -1.387778780781445676E-14, -24.99999999999998224, 0.000000000000000000 ) ) ;
#7704=FACE_OUTER_BOUND ( 'NONE', #22535, .T. ) ;
#7728=EDGE_CURVE ( 'NONE', #15995, #10242, #10113, .T. ) ;
#7935=UNCERTAINTY_MEASURE_WITH_UNIT (LENGTH_MEASURE( 1.000000000000000082E-05 ), #9094, 'distance_accuracy_value', 'NONE');
#8086=ORIENTED_EDGE ( 'NONE', *, *, #14460, .F. ) ;
#8117=ORIENTED_EDGE ( 'NONE', *, *, #3615, .T. ) ;
#8221=AXIS2_PLACEMENT_3D ( 'NONE', #13110, #19944, #16738 ) ;
#8271=ORIENTED_EDGE ( 'NONE', *, *, #17717, .T. ) ;
#8309=CARTESIAN_POINT ( 'NONE',  ( -1.387778780781445676E-14, -24.99999999999998224, 0.000000000000000000 ) ) ;
#8324=ORIENTED_EDGE ( 'NONE', *, *, #6172, .F. ) ;
#8356=PRODUCT_DEFINITION_SHAPE ( 'NONE', 'NONE',  #3448 ) ;
#8357=DIRECTION ( 'NONE',  ( -2.775557561562883647E-17, 3.406761633869147840E-16, -1.000000000000000000 ) ) ;
#8363=CARTESIAN_POINT ( 'NONE',  ( -1.354447211139183087E-14, 6.219541108242056490E-16, 4.750000000000000000 ) ) ;
#8419=ORIENTED_EDGE ( 'NONE', *, *, #12101, .T. ) ;
#8510=ADVANCED_FACE ( 'NONE', ( #13334 ), #480, .T. ) ;
#8597=PRESENTATION_STYLE_ASSIGNMENT (( #17526 ) ) ;
#8614=FACE_OUTER_BOUND ( 'NONE', #21580, .T. ) ;
#8636=EDGE_LOOP ( 'NONE', ( #10185, #11818, #19779, #20770 ) ) ;
#8648=FACE_OUTER_BOUND ( 'NONE', #3233, .T. ) ;
#8675=CARTESIAN_POINT ( 'NONE',  ( 0.000000000000000000, -14.99999999999997513, -1.387778780781445676E-14 ) ) ;
#8701=DIRECTION ( 'NONE',  ( 2.775557561562883955E-17, -3.406761633869148826E-16, 1.000000000000000000 ) ) ;
#8706=AXIS2_PLACEMENT_3D ( 'NONE', #15776, #18227, #2095 ) ;
#8808=DIRECTION ( 'NONE',  ( -2.775557561562883955E-17, 3.406761633869148826E-16, -1.000000000000000000 ) ) ;
#8844=ORIENTED_EDGE ( 'NONE', *, *, #9603, .F. ) ;
#8856=LINE ( 'NONE', #9430, #7535 ) ;
#8870=ORIENTED_EDGE ( 'NONE', *, *, #20624, .F. ) ;
#8884=VECTOR ( 'NONE', #20212, 1000.000000000000000 ) ;
#8922=SURFACE_STYLE_FILL_AREA ( #7169 ) ;
#8945=DIRECTION ( 'NONE',  ( -2.172745813409349776E-17, 1.000000000000000000, -1.309377075419428048E-16 ) ) ;
#9002=DIRECTION ( 'NONE',  ( 2.172745813409349776E-17, -1.000000000000000000, 1.309377075419428048E-16 ) ) ;
#9094=( LENGTH_UNIT ( ) NAMED_UNIT ( * ) SI_UNIT ( .MILLI., .METRE. ) );
#9108=ADVANCED_FACE ( 'NONE', ( #22709 ), #23060, .T. ) ;
#9228=EDGE_CURVE ( 'NONE', #2293, #2880, #4638, .T. ) ;
#9239=ORIENTED_EDGE ( 'NONE', *, *, #13750, .T. ) ;
#9251=COLOUR_RGB ( '', 0.08235294, 0.09019608, 0.10196078) ;
#9268=VECTOR ( 'NONE', #19829, 1000.000000000000114 ) ;
#9282=CARTESIAN_POINT ( 'NONE',  ( -6.938893903907228378E-15, -22.91099746826335348, -1.387778780781445676E-14 ) ) ;
#9284=COLOUR_RGB ( '', 0.66274510, 0.83137255, 0.94901961) ;
#9430=CARTESIAN_POINT ( 'NONE',  ( 1.318389841742373392E-16, -14.99999999999997691, 4.749999999999999112 ) ) ;
#9467=LINE ( 'NONE', #14647, #9268 ) ;
#9474=CIRCLE ( 'NONE', #10955, 4.750000000000013323 ) ;
#9485=CARTESIAN_POINT ( 'NONE',  ( -1.354447211139180878E-14, -14.99999999999997513, 4.749999999999985789 ) ) ;
#9526=AXIS2_PLACEMENT_3D ( 'NONE', #13521, #17029, #13754 ) ;
#9603=EDGE_CURVE ( 'NONE', #20996, #5042, #13852, .T. ) ;
#9701=DIRECTION ( 'NONE',  ( -2.172745813409348851E-17, 1.000000000000000000, 3.406761633869148826E-16 ) ) ;
#9726=CARTESIAN_POINT ( 'NONE',  ( 0.000000000000000000, -14.99999999999997513, -1.387778780781445676E-14 ) ) ;
#9798=ADVANCED_FACE ( 'NONE', ( #3829 ), #12870, .T. ) ;
#9814=VECTOR ( 'NONE', #21969, 1000.000000000000000 ) ;
#10038=CIRCLE ( 'NONE', #18299, 4.750000000000013323 ) ;
#10101=AXIS2_PLACEMENT_3D ( 'NONE', #15805, #23133, #7017 ) ;
#10113=CIRCLE ( 'NONE', #20259, 2.500000000000006661 ) ;
#10185=ORIENTED_EDGE ( 'NONE', *, *, #5772, .F. ) ;
#10188=EDGE_CURVE ( 'NONE', #7568, #10218, #15872, .T. ) ;
#10218=VERTEX_POINT ( 'NONE', #3697 ) ;
#10242=VERTEX_POINT ( 'NONE', #5830 ) ;
#10331=CARTESIAN_POINT ( 'NONE',  ( -1.387778780781445676E-14, -8.271819572847247670, 0.000000000000000000 ) ) ;
#10355=SURFACE_SIDE_STYLE ('',( #19300 ) ) ;
#10429=EDGE_LOOP ( 'NONE', ( #3822, #21238, #8324, #7599 ) ) ;
#10629=EDGE_LOOP ( 'NONE', ( #14598, #11463, #12215, #21291 ) ) ;
#10682=( NAMED_UNIT ( * ) SI_UNIT ( $, .STERADIAN. ) SOLID_ANGLE_UNIT ( ) );
#10692=DIRECTION ( 'NONE',  ( -2.775557561562883647E-17, 3.652049423109057473E-16, -1.000000000000000000 ) ) ;
#10712=PRODUCT_CONTEXT ( 'NONE', #22871, 'mechanical' ) ;
#10955=AXIS2_PLACEMENT_3D ( 'NONE', #8675, #19497, #11962 ) ;
#10957=EDGE_CURVE ( 'NONE', #16094, #13530, #1583, .T. ) ;
#10977=VECTOR ( 'NONE', #1502, 1000.000000000000114 ) ;
#10985=DIRECTION ( 'NONE',  ( 1.714307746994311415E-19, -0.7904150521752424385, -0.6125716654358157598 ) ) ;
#11012=DIRECTION ( 'NONE',  ( -2.775557561562890735E-17, 3.352716401118095686E-16, -1.000000000000000000 ) ) ;
#11065=ADVANCED_FACE ( 'NONE', ( #18313 ), #2303, .T. ) ;
#11082=( NAMED_UNIT ( * ) PLANE_ANGLE_UNIT ( ) SI_UNIT ( $, .RADIAN. ) );
#11091=ORIENTED_EDGE ( 'NONE', *, *, #17149, .F. ) ;
#11109=ORIENTED_EDGE ( 'NONE', *, *, #6238, .F. ) ;
#11191=DIRECTION ( 'NONE',  ( 2.775557561562824791E-17, 0.000000000000000000, 1.000000000000000000 ) ) ;
#11211=ORIENTED_EDGE ( 'NONE', *, *, #16419, .T. ) ;
#11219=AXIS2_PLACEMENT_3D ( 'NONE', #1397, #19508, #8808 ) ;
#11311=EDGE_LOOP ( 'NONE', ( #13528, #6271, #3432, #860 ) ) ;
#11327=CONICAL_SURFACE ( 'NONE', #2317, 12.50000000000003375, 0.1651486774146268266 ) ;
#11383=EDGE_CURVE ( 'NONE', #7568, #21501, #2738, .T. ) ;
#11463=ORIENTED_EDGE ( 'NONE', *, *, #10188, .F. ) ;
#11473=FACE_OUTER_BOUND ( 'NONE', #5288, .T. ) ;
#11591=CARTESIAN_POINT ( 'NONE',  ( 6.827186199083545087E-16, -11.33467790002633002, -7.208584908080457154 ) ) ;
#11693=EDGE_LOOP ( 'NONE', ( #14970, #3260, #22708, #628 ) ) ;
#11745=EDGE_CURVE ( 'NONE', #16893, #19599, #20047, .T. ) ;
#11818=ORIENTED_EDGE ( 'NONE', *, *, #15718, .T. ) ;
#11820=DIRECTION ( 'NONE',  ( 2.172745813409348851E-17, -1.000000000000000000, -3.406761633869148826E-16 ) ) ;
#11882=DIRECTION ( 'NONE',  ( -2.775557561562883647E-17, 3.406761633869147840E-16, -1.000000000000000000 ) ) ;
#11919=CIRCLE ( 'NONE', #14544, 4.750000000000013323 ) ;
#11927=DIRECTION ( 'NONE',  ( -2.775557561562883955E-17, 3.406761633869148826E-16, -1.000000000000000000 ) ) ;
#11950=CIRCLE ( 'NONE', #23248, 4.999999999999999112 ) ;
#11956=ORIENTED_EDGE ( 'NONE', *, *, #3919, .T. ) ;
#11962=DIRECTION ( 'NONE',  ( -2.775557561562883647E-17, 3.652049423109057473E-16, -1.000000000000000000 ) ) ;
#11967=AXIS2_PLACEMENT_3D ( 'NONE', #22050, #14981, #20291 ) ;
#12063=DIRECTION ( 'NONE',  ( -2.172745813409349776E-17, 1.000000000000000000, -1.309377075419428048E-16 ) ) ;
#12066=CARTESIAN_POINT ( 'NONE',  ( -6.555066805945576033E-15, -12.15667283655308850, 12.14055452724117856 ) ) ;
#12101=EDGE_CURVE ( 'NONE', #2293, #22503, #21506, .T. ) ;
#12102=DIRECTION ( 'NONE',  ( 2.172745813409349776E-17, -1.000000000000000000, 1.309377075419428048E-16 ) ) ;
#12110=FILL_AREA_STYLE ('',( #21076 ) ) ;
#12132=DIRECTION ( 'NONE',  ( -2.775557561562890735E-17, 3.352716401118095686E-16, -1.000000000000000000 ) ) ;
#12165=CARTESIAN_POINT ( 'NONE',  ( 0.000000000000000000, -14.99999999999997513, -1.387778780781445676E-14 ) ) ;
#12200=PRESENTATION_STYLE_ASSIGNMENT (( #15844 ) ) ;
#12215=ORIENTED_EDGE ( 'NONE', *, *, #11383, .T. ) ;
#12233=STYLED_ITEM ( 'NONE', ( #12200 ), #21257 ) ;
#12280=CARTESIAN_POINT ( 'NONE',  ( -3.111695183146356892E-17, -14.99999999999997513, 4.749999999999985789 ) ) ;
#12298=ADVANCED_FACE ( 'NONE', ( #7488 ), #3544, .T. ) ;
#12307=CARTESIAN_POINT ( 'NONE',  ( 7.135462137692308706E-16, -1.618211776087849834E-15, 4.750000000000013323 ) ) ;
#12356=ORIENTED_EDGE ( 'NONE', *, *, #22939, .T. ) ;
#12404=CARTESIAN_POINT ( 'NONE',  ( -1.318389841742373392E-16, 1.618211776087849834E-15, -4.750000000000013323 ) ) ;
#12418=ADVANCED_FACE ( 'NONE', ( #22652, #16872 ), #20782, .F. ) ;
#12608=DIRECTION ( 'NONE',  ( -2.172745813409349776E-17, 1.000000000000000000, -1.309377075419428048E-16 ) ) ;
#12609=DIRECTION ( 'NONE',  ( -2.775557561562902444E-17, 0.000000000000000000, -1.000000000000000000 ) ) ;
#12728=CARTESIAN_POINT ( 'NONE',  ( -1.387778780781445676E-14, -24.99999999999998224, 0.000000000000000000 ) ) ;
#12738=SURFACE_SIDE_STYLE ('',( #16252 ) ) ;
#12868=AXIS2_PLACEMENT_3D ( 'NONE', #22892, #6545, #17105 ) ;
#12870=TOROIDAL_SURFACE ( 'NONE', #17754, 7.208584908080424292, 5.000000000000000000 ) ;
#12902=VECTOR ( 'NONE', #10985, 999.9999999999998863 ) ;
#13012=ORIENTED_EDGE ( 'NONE', *, *, #12101, .F. ) ;
#13087=FILL_AREA_STYLE ('',( #14729 ) ) ;
#13110=CARTESIAN_POINT ( 'NONE',  ( 0.000000000000000000, -11.33467790002633180, -1.387778780781445676E-14 ) ) ;
#13114=CARTESIAN_POINT ( 'NONE',  ( -10.00000000000000888, -24.99999999999994671, 0.000000000000000000 ) ) ;
#13334=FACE_OUTER_BOUND ( 'NONE', #14195, .T. ) ;
#13357=ORIENTED_EDGE ( 'NONE', *, *, #14971, .T. ) ;
#13446=AXIS2_PLACEMENT_3D ( 'NONE', #5153, #16188, #17734 ) ;
#13521=CARTESIAN_POINT ( 'NONE',  ( 2.081668171172168513E-14, 10.00000000000000533, 0.000000000000000000 ) ) ;
#13528=ORIENTED_EDGE ( 'NONE', *, *, #20560, .F. ) ;
#13530=VERTEX_POINT ( 'NONE', #15583 ) ;
#13551=CARTESIAN_POINT ( 'NONE',  ( 0.000000000000000000, 0.000000000000000000, 0.000000000000000000 ) ) ;
#13600=CARTESIAN_POINT ( 'NONE',  ( -1.300449337779986339E-16, -8.271819572847249447, -11.16066016895666380 ) ) ;
#13603=DIRECTION ( 'NONE',  ( 2.775557561562886113E-17, -2.775557561562883955E-16, 1.000000000000000000 ) ) ;
#13649=ORIENTED_EDGE ( 'NONE', *, *, #18423, .F. ) ;
#13698=CLOSED_SHELL ( 'NONE', ( #9108, #3030, #2905, #12298, #19709, #18039, #6285, #4133, #15277, #8510, #9798, #3038 ) ) ;
#13750=EDGE_CURVE ( 'NONE', #13530, #16094, #19163, .T. ) ;
#13754=DIRECTION ( 'NONE',  ( -2.775557561562824791E-17, 0.000000000000000000, -1.000000000000000000 ) ) ;
#13764=CARTESIAN_POINT ( 'NONE',  ( 1.387778780781445676E-14, -22.49999999999995737, -2.775557561562891351E-14 ) ) ;
#13827=DIRECTION ( 'NONE',  ( 2.172745813409348851E-17, -1.000000000000000000, -3.406761633869148826E-16 ) ) ;
#13852=LINE ( 'NONE', #12307, #10977 ) ;
#13865=CYLINDRICAL_SURFACE ( 'NONE', #9526, 2.500000000000006661 ) ;
#13900=EDGE_CURVE ( 'NONE', #22503, #16146, #16148, .T. ) ;
#13927=ORIENTED_EDGE ( 'NONE', *, *, #3116, .F. ) ;
#13939=FACE_OUTER_BOUND ( 'NONE', #8636, .T. ) ;
#14015=EDGE_LOOP ( 'NONE', ( #13927, #21528 ) ) ;
#14058=FACE_OUTER_BOUND ( 'NONE', #22121, .T. ) ;
#14072=SHAPE_REPRESENTATION ( 'Rubber Head', ( #22115 ), #20270 ) ;
#14126=EDGE_CURVE ( 'NONE', #2880, #16146, #8856, .T. ) ;
#14167=EDGE_LOOP ( 'NONE', ( #11109, #4427, #20037, #8117 ) ) ;
#14195=EDGE_LOOP ( 'NONE', ( #8844, #7407, #8271, #20650 ) ) ;
#14225=VERTEX_POINT ( 'NONE', #21899 ) ;
#14233=FACE_OUTER_BOUND ( 'NONE', #19010, .T. ) ;
#14325=DIRECTION ( 'NONE',  ( 2.172745813409349776E-17, -1.000000000000000000, 1.309377075419428048E-16 ) ) ;
#14377=FACE_OUTER_BOUND ( 'NONE', #11311, .T. ) ;
#14460=EDGE_CURVE ( 'NONE', #16146, #22503, #16178, .T. ) ;
#14539=DIRECTION ( 'NONE',  ( -2.172745813409349776E-17, 1.000000000000000000, -1.309377075419428048E-16 ) ) ;
#14544=AXIS2_PLACEMENT_3D ( 'NONE', #5537, #21545, #3424 ) ;
#14598=ORIENTED_EDGE ( 'NONE', *, *, #21927, .F. ) ;
#14647=CARTESIAN_POINT ( 'NONE',  ( -6.591949208711866959E-15, -9.999999999999971578, 12.50000000000003375 ) ) ;
#14649=AXIS2_PLACEMENT_3D ( 'NONE', #18062, #4149, #21822 ) ;
#14729=FILL_AREA_STYLE_COLOUR ( '', #6744 ) ;
#14852=( LENGTH_UNIT ( ) NAMED_UNIT ( * ) SI_UNIT ( .MILLI., .METRE. ) );
#14970=ORIENTED_EDGE ( 'NONE', *, *, #3919, .F. ) ;
#14971=EDGE_CURVE ( 'NONE', #21501, #14225, #21104, .T. ) ;
#14981=DIRECTION ( 'NONE',  ( -2.172745813409349776E-17, 1.000000000000000000, -1.309377075419428048E-16 ) ) ;
#15073=CARTESIAN_POINT ( 'NONE',  ( 0.000000000000000000, 0.000000000000000000, 0.000000000000000000 ) ) ;
#15084=AXIS2_PLACEMENT_3D ( 'NONE', #9726, #20433, #16759 ) ;
#15134=ADVANCED_FACE ( 'NONE', ( #11473 ), #2539, .T. ) ;
#15172=ORIENTED_EDGE ( 'NONE', *, *, #6172, .T. ) ;
#15247=ORIENTED_EDGE ( 'NONE', *, *, #20560, .T. ) ;
#15277=ADVANCED_FACE ( 'NONE', ( #13939 ), #11327, .T. ) ;
#15385=FACE_OUTER_BOUND ( 'NONE', #14167, .T. ) ;
#15498=AXIS2_PLACEMENT_3D ( 'NONE', #16503, #1924, #3810 ) ;
#15583=CARTESIAN_POINT ( 'NONE',  ( -5.742213840172610633E-15, -12.15667283655309205, -12.14055452724117679 ) ) ;
#15649=EDGE_LOOP ( 'NONE', ( #8086, #22845 ) ) ;
#15672=DIRECTION ( 'NONE',  ( 1.000000000000000000, 2.172745813409351317E-17, 9.470910429910635790E-17 ) ) ;
#15718=EDGE_CURVE ( 'NONE', #14225, #21501, #16941, .T. ) ;
#15776=CARTESIAN_POINT ( 'NONE',  ( 0.000000000000000000, -14.99999999999997513, -1.387778780781445676E-14 ) ) ;
#15805=CARTESIAN_POINT ( 'NONE',  ( 0.000000000000000000, 0.000000000000000000, 0.000000000000000000 ) ) ;
#15834=ADVANCED_FACE ( 'NONE', ( #8614 ), #21451, .T. ) ;
#15844=SURFACE_STYLE_USAGE ( .BOTH. , #16192 ) ;
#15872=CIRCLE ( 'NONE', #18903, 7.882182279042429407 ) ;
#15888=DIRECTION ( 'NONE',  ( -2.172745813409349776E-17, 1.000000000000000000, -1.309377075419428048E-16 ) ) ;
#15904=CARTESIAN_POINT ( 'NONE',  ( 2.000784234979076174E-16, -11.33467790002633357, 7.208584908080428733 ) ) ;
#15911=VERTEX_POINT ( 'NONE', #6102 ) ;
#15995=VERTEX_POINT ( 'NONE', #20228 ) ;
#16079=( NAMED_UNIT ( * ) PLANE_ANGLE_UNIT ( ) SI_UNIT ( $, .RADIAN. ) );
#16094=VERTEX_POINT ( 'NONE', #12066 ) ;
#16115=STYLED_ITEM ( 'NONE', ( #18386 ), #202 ) ;
#16128=DIRECTION ( 'NONE',  ( -2.775557561562902444E-17, 0.000000000000000000, -1.000000000000000000 ) ) ;
#16137=EDGE_CURVE ( 'NONE', #2880, #2293, #9474, .T. ) ;
#16146=VERTEX_POINT ( 'NONE', #17725 ) ;
#16148=CIRCLE ( 'NONE', #401, 4.750000000000013323 ) ;
#16168=CARTESIAN_POINT ( 'NONE',  ( 0.000000000000000000, 0.000000000000000000, 0.000000000000000000 ) ) ;
#16178=CIRCLE ( 'NONE', #22578, 4.750000000000013323 ) ;
#16188=DIRECTION ( 'NONE',  ( -2.172745813409349776E-17, 1.000000000000000000, -1.309377075419428048E-16 ) ) ;
#16192=SURFACE_SIDE_STYLE ('',( #8922 ) ) ;
#16252=SURFACE_STYLE_FILL_AREA ( #13087 ) ;
#16269=EDGE_LOOP ( 'NONE', ( #3515, #16752, #12356, #20483 ) ) ;
#16356=DIRECTION ( 'NONE',  ( -2.172745813409349776E-17, 1.000000000000000000, -1.309377075419428048E-16 ) ) ;
#16419=EDGE_CURVE ( 'NONE', #2526, #21123, #23019, .T. ) ;
#16427=ADVANCED_FACE ( 'NONE', ( #14058 ), #22772, .T. ) ;
#16430=ORIENTED_EDGE ( 'NONE', *, *, #22175, .T. ) ;
#16493=VERTEX_POINT ( 'NONE', #13600 ) ;
#16503=CARTESIAN_POINT ( 'NONE',  ( 1.409656231407658705E-14, -22.49999999999996092, 7.882182279042401873 ) ) ;
#16597=ORIENTED_EDGE ( 'NONE', *, *, #3615, .F. ) ;
#16738=DIRECTION ( 'NONE',  ( 2.775557561562883031E-17, 1.309377075419427801E-16, 1.000000000000000000 ) ) ;
#16752=ORIENTED_EDGE ( 'NONE', *, *, #10957, .F. ) ;
#16759=DIRECTION ( 'NONE',  ( 2.775557561562883647E-17, -3.652049423109057473E-16, 1.000000000000000000 ) ) ;
#16761=DIRECTION ( 'NONE',  ( 2.172745813409349776E-17, -1.000000000000000000, 1.309377075419428048E-16 ) ) ;
#16764=CARTESIAN_POINT ( 'NONE',  ( 2.074729277268261285E-14, 10.00000000000000533, -2.500000000000006661 ) ) ;
#16769=ORIENTED_EDGE ( 'NONE', *, *, #13900, .T. ) ;
#16786=CIRCLE ( 'NONE', #4386, 11.16066016895667268 ) ;
#16872=FACE_OUTER_BOUND ( 'NONE', #15649, .T. ) ;
#16893=VERTEX_POINT ( 'NONE', #5450 ) ;
#16941=CIRCLE ( 'NONE', #19974, 10.34816708862279633 ) ;
#17029=DIRECTION ( 'NONE',  ( 2.172745813409349776E-17, -1.000000000000000000, 1.309377075419428048E-16 ) ) ;
#17030=DIRECTION ( 'NONE',  ( 2.775557561562891043E-17, -3.108639542312977099E-16, 1.000000000000000000 ) ) ;
#17051=AXIS2_PLACEMENT_3D ( 'NONE', #17099, #11820, #11927 ) ;
#17099=CARTESIAN_POINT ( 'NONE',  ( 0.000000000000000000, 0.000000000000000000, 0.000000000000000000 ) ) ;
#17105=DIRECTION ( 'NONE',  ( -2.775557561562883647E-17, 3.652049423109057473E-16, -1.000000000000000000 ) ) ;
#17149=EDGE_CURVE ( 'NONE', #20996, #15911, #22292, .T. ) ;
#17340=EDGE_CURVE ( 'NONE', #16493, #5042, #5775, .T. ) ;
#17526=SURFACE_STYLE_USAGE ( .BOTH. , #10355 ) ;
#17586=DIRECTION ( 'NONE',  ( -2.172745813409349776E-17, 1.000000000000000000, -1.309377075419428048E-16 ) ) ;
#17622=LINE ( 'NONE', #17865, #19060 ) ;
#17632=DIRECTION ( 'NONE',  ( 2.172745813409349776E-17, -1.000000000000000000, 1.309377075419428048E-16 ) ) ;
#17670=CARTESIAN_POINT ( 'NONE',  ( -1.387778780781445676E-14, -24.99999999999998224, 0.000000000000000000 ) ) ;
#17717=EDGE_CURVE ( 'NONE', #15911, #16493, #3813, .T. ) ;
#17725=CARTESIAN_POINT ( 'NONE',  ( -3.111695183146366136E-17, 6.219541108242305968E-16, 4.750000000000000000 ) ) ;
#17734=DIRECTION ( 'NONE',  ( 2.775557561562883955E-17, -3.406761633869148333E-16, 1.000000000000000000 ) ) ;
#17739=FILL_AREA_STYLE_COLOUR ( '', #9251 ) ;
#17754=AXIS2_PLACEMENT_3D ( 'NONE', #18421, #14539, #21963 ) ;
#17836=DIRECTION ( 'NONE',  ( 2.775557561562824791E-17, 0.000000000000000000, 1.000000000000000000 ) ) ;
#17855=CARTESIAN_POINT ( 'NONE',  ( -6.938893903907228378E-15, -12.15667283655309028, 0.000000000000000000 ) ) ;
#17865=CARTESIAN_POINT ( 'NONE',  ( 2.119223235054759529E-14, 10.00000000000000533, 2.500000000000006661 ) ) ;
#17973=DIRECTION ( 'NONE',  ( 2.172745813409349776E-17, -1.000000000000000000, 1.309377075419428048E-16 ) ) ;
#18039=ADVANCED_FACE ( 'NONE', ( #14377 ), #5564, .F. ) ;
#18062=CARTESIAN_POINT ( 'NONE',  ( -6.938893903907228378E-15, -12.15667283655309028, 0.000000000000000000 ) ) ;
#18106=EDGE_LOOP ( 'NONE', ( #16597, #21113 ) ) ;
#18207=DIRECTION ( 'NONE',  ( 2.172745813409349776E-17, -1.000000000000000000, 1.309377075419428048E-16 ) ) ;
#18214=LINE ( 'NONE', #16764, #8884 ) ;
#18227=DIRECTION ( 'NONE',  ( -2.172745813409349776E-17, 1.000000000000000000, -1.309377075419428048E-16 ) ) ;
#18267=ORIENTED_EDGE ( 'NONE', *, *, #14126, .F. ) ;
#18299=AXIS2_PLACEMENT_3D ( 'NONE', #13551, #18724, #1095 ) ;
#18313=FACE_OUTER_BOUND ( 'NONE', #11693, .T. ) ;
#18377=CIRCLE ( 'NONE', #5608, 2.500000000000006661 ) ;
#18386=PRESENTATION_STYLE_ASSIGNMENT (( #19924 ) ) ;
#18421=CARTESIAN_POINT ( 'NONE',  ( 0.000000000000000000, -11.33467790002633180, -1.387778780781445676E-14 ) ) ;
#18423=EDGE_CURVE ( 'NONE', #15911, #21123, #22487, .T. ) ;
#18535=CARTESIAN_POINT ( 'NONE',  ( -6.938893903907228378E-15, -9.999999999999968026, 0.000000000000000000 ) ) ;
#18724=DIRECTION ( 'NONE',  ( 2.172745813409349776E-17, -1.000000000000000000, 1.309377075419428048E-16 ) ) ;
#18757=ADVANCED_FACE ( 'NONE', ( #15385 ), #13865, .T. ) ;
#18771=PRODUCT_DEFINITION_FORMATION_WITH_SPECIFIED_SOURCE ( 'ANY', '', #4976, .NOT_KNOWN. ) ;
#18785=CARTESIAN_POINT ( 'NONE',  ( -6.463109109390148576E-15, -22.91099746826335348, 10.34816708862275547 ) ) ;
#18819=ORIENTED_EDGE ( 'NONE', *, *, #14126, .T. ) ;
#18883=AXIS2_PLACEMENT_3D ( 'NONE', #3832, #18207, #2073 ) ;
#18903=AXIS2_PLACEMENT_3D ( 'NONE', #7698, #9002, #5473 ) ;
#18981=DIRECTION ( 'NONE',  ( -2.775557561562883647E-17, 3.406761633869147840E-16, -1.000000000000000000 ) ) ;
#19010=EDGE_LOOP ( 'NONE', ( #2002, #11956 ) ) ;
#19060=VECTOR ( 'NONE', #14325, 1000.000000000000000 ) ;
#19150=APPLICATION_CONTEXT ( 'automotive_design' ) ;
#19163=CIRCLE ( 'NONE', #14649, 12.14055452724117856 ) ;
#19287=CARTESIAN_POINT ( 'NONE',  ( 2.081668171172168513E-14, 10.00000000000000533, 0.000000000000000000 ) ) ;
#19300=SURFACE_STYLE_FILL_AREA ( #12110 ) ;
#19356=CARTESIAN_POINT ( 'NONE',  ( -6.938893903907228378E-15, -9.999999999999968026, 0.000000000000000000 ) ) ;
#19415=ORIENTED_EDGE ( 'NONE', *, *, #11383, .F. ) ;
#19497=DIRECTION ( 'NONE',  ( 2.172745813409349776E-17, -1.000000000000000000, 1.309377075419428048E-16 ) ) ;
#19508=DIRECTION ( 'NONE',  ( 2.172745813409348851E-17, -1.000000000000000000, -3.406761633869148826E-16 ) ) ;
#19524=PLANE ( 'NONE',  #21635 ) ;
#19529=CARTESIAN_POINT ( 'NONE',  ( 0.000000000000000000, 0.000000000000000000, 0.000000000000000000 ) ) ;
#19599=VERTEX_POINT ( 'NONE', #7329 ) ;
#19679=AXIS2_PLACEMENT_3D ( 'NONE', #13764, #4574, #4464 ) ;
#19709=ADVANCED_FACE ( 'NONE', ( #5562 ), #3566, .F. ) ;
#19779=ORIENTED_EDGE ( 'NONE', *, *, #21745, .T. ) ;
#19829=DIRECTION ( 'NONE',  ( -1.686884416050044188E-17, 0.9863939238321436376, 0.1643989873053578188 ) ) ;
#19888=( LENGTH_UNIT ( ) NAMED_UNIT ( * ) SI_UNIT ( .MILLI., .METRE. ) );
#19899=( GEOMETRIC_REPRESENTATION_CONTEXT ( 3 ) GLOBAL_UNCERTAINTY_ASSIGNED_CONTEXT ( ( #19950 ) ) GLOBAL_UNIT_ASSIGNED_CONTEXT ( ( #14852, #11082, #7452 ) ) REPRESENTATION_CONTEXT ( 'NONE', 'WORKASPACE' ) );
#19924=SURFACE_STYLE_USAGE ( .BOTH. , #12738 ) ;
#19944=DIRECTION ( 'NONE',  ( -2.172745813409349776E-17, 1.000000000000000000, -1.309377075419428048E-16 ) ) ;
#19950=UNCERTAINTY_MEASURE_WITH_UNIT (LENGTH_MEASURE( 1.000000000000000082E-05 ), #14852, 'distance_accuracy_value', 'NONE');
#19974=AXIS2_PLACEMENT_3D ( 'NONE', #9282, #15888, #12132 ) ;
#20037=ORIENTED_EDGE ( 'NONE', *, *, #21380, .T. ) ;
#20047=CIRCLE ( 'NONE', #4237, 2.500000000000006661 ) ;
#20150=SHAPE_REPRESENTATION_RELATIONSHIP ( 'NONE' , 'NONE' ,  #14072, #202 ) ;
#20153=UNCERTAINTY_MEASURE_WITH_UNIT (LENGTH_MEASURE( 1.000000000000000082E-05 ), #1627, 'distance_accuracy_value', 'NONE');
#20179=PRODUCT_DEFINITION_CONTEXT ( 'detailed design', #19150, 'design' ) ;
#20212=DIRECTION ( 'NONE',  ( 2.172745813409349776E-17, -1.000000000000000000, 1.309377075419428048E-16 ) ) ;
#20228=CARTESIAN_POINT ( 'NONE',  ( 2.130086964121800697E-14, 3.273442688548750448E-16, 2.500000000000000000 ) ) ;
#20259=AXIS2_PLACEMENT_3D ( 'NONE', #16168, #22906, #3381 ) ;
#20270=( GEOMETRIC_REPRESENTATION_CONTEXT ( 3 ) GLOBAL_UNCERTAINTY_ASSIGNED_CONTEXT ( ( #7935 ) ) GLOBAL_UNIT_ASSIGNED_CONTEXT ( ( #9094, #6033, #5690 ) ) REPRESENTATION_CONTEXT ( 'NONE', 'WORKASPACE' ) );
#20291=DIRECTION ( 'NONE',  ( 2.775557561562885188E-17, 1.309377075419427801E-16, 1.000000000000000000 ) ) ;
#20414=AXIS2_PLACEMENT_3D ( 'NONE', #963, #20604, #8357 ) ;
#20433=DIRECTION ( 'NONE',  ( -2.172745813409349776E-17, 1.000000000000000000, -1.309377075419428048E-16 ) ) ;
#20436=AXIS2_PLACEMENT_3D ( 'NONE', #3297, #17632, #10692 ) ;
#20437=DIRECTION ( 'NONE',  ( 2.775557561562886729E-17, -4.401632478328199173E-16, 1.000000000000000000 ) ) ;
#20470=VECTOR ( 'NONE', #20852, 1000.000000000000000 ) ;
#20483=ORIENTED_EDGE ( 'NONE', *, *, #17340, .F. ) ;
#20560=EDGE_CURVE ( 'NONE', #20996, #2526, #437, .T. ) ;
#20604=DIRECTION ( 'NONE',  ( 2.172745813409349776E-17, -1.000000000000000000, 1.309377075419428048E-16 ) ) ;
#20624=EDGE_CURVE ( 'NONE', #10218, #7568, #5692, .T. ) ;
#20650=ORIENTED_EDGE ( 'NONE', *, *, #17340, .T. ) ;
#20655=ORIENTED_EDGE ( 'NONE', *, *, #20624, .T. ) ;
#20725=CARTESIAN_POINT ( 'NONE',  ( -1.400962679198869567E-14, -24.99999999999998224, -4.750000000000013323 ) ) ;
#20770=ORIENTED_EDGE ( 'NONE', *, *, #10957, .T. ) ;
#20782=PLANE ( 'NONE',  #17051 ) ;
#20852=DIRECTION ( 'NONE',  ( 2.172745813409349776E-17, -1.000000000000000000, 1.309377075419428048E-16 ) ) ;
#20996=VERTEX_POINT ( 'NONE', #8363 ) ;
#21014=MANIFOLD_SOLID_BREP ( 'Fillet2', #13698 ) ;
#21076=FILL_AREA_STYLE_COLOUR ( '', #9284 ) ;
#21104=CIRCLE ( 'NONE', #3792, 10.34816708862279633 ) ;
#21113=ORIENTED_EDGE ( 'NONE', *, *, #7728, .F. ) ;
#21123=VERTEX_POINT ( 'NONE', #3871 ) ;
#21130=CARTESIAN_POINT ( 'NONE',  ( 1.856282835930036383E-15, -8.271819572847245894, 11.16066016895665669 ) ) ;
#21139=AXIS2_PLACEMENT_3D ( 'NONE', #12165, #13827, #6426 ) ;
#21238=ORIENTED_EDGE ( 'NONE', *, *, #2658, .T. ) ;
#21257=MANIFOLD_SOLID_BREP ( 'Boss-Extrude2', #23095 ) ;
#21291=ORIENTED_EDGE ( 'NONE', *, *, #15718, .F. ) ;
#21380=EDGE_CURVE ( 'NONE', #16893, #10242, #18214, .T. ) ;
#21387=TOROIDAL_SURFACE ( 'NONE', #11967, 7.882182279042408979, 2.500000000000000000 ) ;
#21402=DIRECTION ( 'NONE',  ( -2.775557561562887961E-17, 2.857733511404945646E-16, -1.000000000000000000 ) ) ;
#21431=CARTESIAN_POINT ( 'NONE',  ( -1.387778780781445676E-14, -8.271819572847247670, 0.000000000000000000 ) ) ;
#21451=CYLINDRICAL_SURFACE ( 'NONE', #8706, 4.750000000000013323 ) ;
#21501=VERTEX_POINT ( 'NONE', #18785 ) ;
#21506=LINE ( 'NONE', #23031, #23084 ) ;
#21528=ORIENTED_EDGE ( 'NONE', *, *, #16419, .F. ) ;
#21545=DIRECTION ( 'NONE',  ( 2.172745813409349776E-17, -1.000000000000000000, 1.309377075419428048E-16 ) ) ;
#21555=SHAPE_DEFINITION_REPRESENTATION ( #8356, #14072 ) ;
#21564=AXIS2_PLACEMENT_3D ( 'NONE', #21431, #8945, #7186 ) ;
#21580=EDGE_LOOP ( 'NONE', ( #13012, #5104, #18819, #22480 ) ) ;
#21635=AXIS2_PLACEMENT_3D ( 'NONE', #19287, #7066, #8701 ) ;
#21745=EDGE_CURVE ( 'NONE', #21501, #16094, #9467, .T. ) ;
#21763=EDGE_LOOP ( 'NONE', ( #8870, #3268, #1607, #19415 ) ) ;
#21822=DIRECTION ( 'NONE',  ( -2.775557561562887961E-17, 2.857733511404945646E-16, -1.000000000000000000 ) ) ;
#21899=CARTESIAN_POINT ( 'NONE',  ( -5.710259475508905133E-15, -22.91099746826335348, -10.34816708862278212 ) ) ;
#21927=EDGE_CURVE ( 'NONE', #10218, #14225, #3280, .T. ) ;
#21963=DIRECTION ( 'NONE',  ( 2.775557561562883031E-17, 1.309377075419427801E-16, 1.000000000000000000 ) ) ;
#21969=DIRECTION ( 'NONE',  ( 2.172745813409349776E-17, -1.000000000000000000, 1.309377075419428048E-16 ) ) ;
#22025=( GEOMETRIC_REPRESENTATION_CONTEXT ( 3 ) GLOBAL_UNCERTAINTY_ASSIGNED_CONTEXT ( ( #20153 ) ) GLOBAL_UNIT_ASSIGNED_CONTEXT ( ( #1627, #16079, #10682 ) ) REPRESENTATION_CONTEXT ( 'NONE', 'WORKASPACE' ) );
#22040=ORIENTED_EDGE ( 'NONE', *, *, #10188, .T. ) ;
#22050=CARTESIAN_POINT ( 'NONE',  ( 1.387778780781445676E-14, -22.49999999999995737, -2.775557561562891351E-14 ) ) ;
#22055=PLANE ( 'NONE',  #2534 ) ;
#22115=AXIS2_PLACEMENT_3D ( 'NONE', #4943, #2963, #5306 ) ;
#22118=CONICAL_SURFACE ( 'NONE', #10101, 4.750000000000013323, 0.6593100683328582123 ) ;
#22121=EDGE_LOOP ( 'NONE', ( #6152, #5494 ) ) ;
#22175=EDGE_CURVE ( 'NONE', #15911, #20996, #10038, .T. ) ;
#22292=CIRCLE ( 'NONE', #20414, 4.750000000000013323 ) ;
#22480=ORIENTED_EDGE ( 'NONE', *, *, #14460, .T. ) ;
#22487=LINE ( 'NONE', #20725, #20470 ) ;
#22503=VERTEX_POINT ( 'NONE', #4889 ) ;
#22535=EDGE_LOOP ( 'NONE', ( #22040, #20655 ) ) ;
#22578=AXIS2_PLACEMENT_3D ( 'NONE', #19529, #12102, #11882 ) ;
#22620=DIRECTION ( 'NONE',  ( 2.172745813409349776E-17, -1.000000000000000000, 1.309377075419428048E-16 ) ) ;
#22650=AXIS2_PLACEMENT_3D ( 'NONE', #15073, #3918, #2501 ) ;
#22652=FACE_BOUND ( 'NONE', #18106, .T. ) ;
#22708=ORIENTED_EDGE ( 'NONE', *, *, #7728, .T. ) ;
#22709=FACE_OUTER_BOUND ( 'NONE', #21763, .T. ) ;
#22755=DIRECTION ( 'NONE',  ( 2.775557561562884572E-17, 0.000000000000000000, 1.000000000000000000 ) ) ;
#22772=PLANE ( 'NONE',  #21139 ) ;
#22845=ORIENTED_EDGE ( 'NONE', *, *, #13900, .F. ) ;
#22871=APPLICATION_CONTEXT ( 'automotive_design' ) ;
#22892=CARTESIAN_POINT ( 'NONE',  ( 0.000000000000000000, -14.99999999999997513, -1.387778780781445676E-14 ) ) ;
#22906=DIRECTION ( 'NONE',  ( -2.172745813409349776E-17, 1.000000000000000000, -1.309377075419428048E-16 ) ) ;
#22939=EDGE_CURVE ( 'NONE', #16094, #5042, #4050, .T. ) ;
#23019=CIRCLE ( 'NONE', #12868, 4.750000000000013323 ) ;
#23031=CARTESIAN_POINT ( 'NONE',  ( 4.498682454207562909E-16, -14.99999999999997335, -4.750000000000026645 ) ) ;
#23060=TOROIDAL_SURFACE ( 'NONE', #19679, 7.882182279042408979, 2.500000000000000000 ) ;
#23084=VECTOR ( 'NONE', #12063, 1000.000000000000000 ) ;
#23095=CLOSED_SHELL ( 'NONE', ( #15134, #11065, #18757, #530, #15834, #16427, #12418 ) ) ;
#23133=DIRECTION ( 'NONE',  ( 2.172745813409349776E-17, -1.000000000000000000, 1.309377075419428048E-16 ) ) ;
#23248=AXIS2_PLACEMENT_3D ( 'NONE', #11591, #4534, #907 ) ;
ENDSEC;
END-ISO-10303-21;
